ISO-10303-21;
HEADER;
FILE_DESCRIPTION (('STEP AP214'),
    '1' );
FILE_NAME ('12. Movable Jaw.step',
    '2026-10-09T14:04:53',
    ( '' ),
    ( '' ),
    'SwSTEP 2.0',
    'SolidWorks 2021',
    '' );
FILE_SCHEMA (( 'AUTOMOTIVE_DESIGN' ));
ENDSEC;

DATA;
#89=DIRECTION ( 'NONE',  ( 0.000000000000000000, 1.000000000000000000, 0.000000000000000000 ) ) ;
#352=FILL_AREA_STYLE ('',( #57023 ) ) ;
#420=( GEOMETRIC_REPRESENTATION_CONTEXT ( 3 ) GLOBAL_UNCERTAINTY_ASSIGNED_CONTEXT ( ( #22603 ) ) GLOBAL_UNIT_ASSIGNED_CONTEXT ( ( #87873, #23154, #22635 ) ) REPRESENTATION_CONTEXT ( 'NONE', 'WORKASPACE' ) );
#677=ORIENTED_EDGE ( 'NONE', *, *, #91818, .T. ) ;
#725=DIRECTION ( 'NONE',  ( 0.000000000000000000, 0.000000000000000000, 1.000000000000000000 ) ) ;
#1058=STYLED_ITEM ( 'NONE', ( #103909 ), #28353 ) ;
#2230=CARTESIAN_POINT ( 'NONE',  ( 0.000000000000000000, 1.500000000000000000, 62.00000000000000000 ) ) ;
#2308=CARTESIAN_POINT ( 'NONE',  ( -1.446302031375384789E-15, 60.76237703744687479, 11.80995232570204045 ) ) ;
#2310=SURFACE_STYLE_FILL_AREA ( #76206 ) ;
#2473=CARTESIAN_POINT ( 'NONE',  ( -4.425930005958662145E-15, 43.22324503868515677, 36.14046114390016839 ) ) ;
#2534=MECHANICAL_DESIGN_GEOMETRIC_PRESENTATION_REPRESENTATION('',(#43885),#61148);
#2691=EDGE_CURVE ( 'NONE', #21078, #3869, #37080, .T. ) ;
#2711=ORIENTED_EDGE ( 'NONE', *, *, #54811, .F. ) ;
#3014=CARTESIAN_POINT ( 'NONE',  ( -3.409519076813957649E-15, 51.11204936430951307, 27.84083606136722366 ) ) ;
#3537=CARTESIAN_POINT ( 'NONE',  ( 8.572527594031464315E-16, 60.00000000000000000, -6.999999999999992895 ) ) ;
#3559=CARTESIAN_POINT ( 'NONE',  ( 72.28092228780033679, 43.22324503868516388, -36.14046114390014708 ) ) ;
#3869=VERTEX_POINT ( 'NONE', #44790 ) ;
#3929=CARTESIAN_POINT ( 'NONE',  ( 0.000000000000000000, 60.33964880548970200, -13.06657876680918662 ) ) ;
#4034=DIRECTION ( 'NONE',  ( 0.000000000000000000, 0.000000000000000000, 1.000000000000000000 ) ) ;
#4090=CARTESIAN_POINT ( 'NONE',  ( 23.61990465140407380, 60.76237703744687479, 11.80995232570204401 ) ) ;
#4451=CARTESIAN_POINT ( 'NONE',  ( -39.18206537991729022, 57.18445727710330573, -19.59103268995865221 ) ) ;
#4573=( GEOMETRIC_REPRESENTATION_CONTEXT ( 3 ) GLOBAL_UNCERTAINTY_ASSIGNED_CONTEXT ( ( #77447 ) ) GLOBAL_UNIT_ASSIGNED_CONTEXT ( ( #69444, #56812, #104437 ) ) REPRESENTATION_CONTEXT ( 'NONE', 'WORKASPACE' ) );
#4624=CARTESIAN_POINT ( 'NONE',  ( 6.136456400494866826E-15, 53.37899725327129374, -25.05398456423234066 ) ) ;
#4673=FILL_AREA_STYLE_COLOUR ( '', #28039 ) ;
#4704=CARTESIAN_POINT ( 'NONE',  ( 0.000000000000000000, 0.000000000000000000, -60.00000000000000000 ) ) ;
#4992=CARTESIAN_POINT ( 'NONE',  ( -50.10796912846466000, 53.37899725327127953, -25.05398456423234066 ) ) ;
#5099=DIRECTION ( 'NONE',  ( 0.000000000000000000, 1.000000000000000000, 0.000000000000000000 ) ) ;
#5114=FILL_AREA_STYLE_COLOUR ( '', #80058 ) ;
#5124=AXIS2_PLACEMENT_3D ( 'NONE', #103324, #66567, #725 ) ;
#5159=FILL_AREA_STYLE_COLOUR ( '', #16390 ) ;
#5354=MECHANICAL_DESIGN_GEOMETRIC_PRESENTATION_REPRESENTATION('',(#103585),#13949);
#5633=SURFACE_STYLE_FILL_AREA ( #64417 ) ;
#5681=FILL_AREA_STYLE_COLOUR ( '', #71007 ) ;
#5718=( NAMED_UNIT ( * ) PLANE_ANGLE_UNIT ( ) SI_UNIT ( $, .RADIAN. ) );
#6036=VERTEX_POINT ( 'NONE', #64638 ) ;
#6295=( LENGTH_UNIT ( ) NAMED_UNIT ( * ) SI_UNIT ( .MILLI., .METRE. ) );
#6365=PLANE ( 'NONE',  #101806 ) ;
#6743=CARTESIAN_POINT ( 'NONE',  ( -0.000000000000000000, 34.25047185182970111, -44.13186320217320713 ) ) ;
#6962=CARTESIAN_POINT ( 'NONE',  ( -0.000000000000000000, 53.37899725327129374, -25.05398456423234066 ) ) ;
#7035=CARTESIAN_POINT ( 'NONE',  ( 0.000000000000000000, 0.000000000000000000, 0.000000000000000000 ) ) ;
#7062=ORIENTED_EDGE ( 'NONE', *, *, #21567, .F. ) ;
#7147=CARTESIAN_POINT ( 'NONE',  ( 0.000000000000000000, 1.500000000000000888, 0.000000000000000000 ) ) ;
#7162=CIRCLE ( 'NONE', #48429, 62.00000000000000000 ) ;
#7481=CARTESIAN_POINT ( 'NONE',  ( 0.000000000000000000, 14.17434517210798184, -56.74723269274520021 ) ) ;
#7706=( NAMED_UNIT ( * ) PLANE_ANGLE_UNIT ( ) SI_UNIT ( $, .RADIAN. ) );
#7793=MECHANICAL_DESIGN_GEOMETRIC_PRESENTATION_REPRESENTATION('',(#97340),#74992);
#7830=B_SPLINE_CURVE_WITH_KNOTS ( 'NONE', 3,
 ( #42871, #75769, #18628, #51487 ),
 .UNSPECIFIED., .F., .F.,
 ( 4, 4 ),
 ( 0.000000000000000000, 1.000000000000000000 ),
 .UNSPECIFIED. ) ;
#8021=CARTESIAN_POINT ( 'NONE',  ( -4.088397730506703056E-15, 46.03420836107012093, 33.38430095398285147 ) ) ;
#8361=ORIENTED_EDGE ( 'NONE', *, *, #42042, .F. ) ;
#8444=PRESENTATION_STYLE_ASSIGNMENT (( #82335 ) ) ;
#8704=DIRECTION ( 'NONE',  ( 0.000000000000000000, 1.000000000000000000, 0.000000000000000000 ) ) ;
#8819=CARTESIAN_POINT ( 'NONE',  ( -6.011841252072294266E-15, 27.55047179872464724, 49.09040922050319011 ) ) ;
#9132=ORIENTED_EDGE ( 'NONE', *, *, #2691, .F. ) ;
#9150=DIRECTION ( 'NONE',  ( 0.000000000000000000, 0.000000000000000000, 1.000000000000000000 ) ) ;
#9357=CARTESIAN_POINT ( 'NONE',  ( 0.000000000000000000, 60.00000000000000000, 6.999999999999992895 ) ) ;
#9944=ORIENTED_EDGE ( 'NONE', *, *, #69013, .F. ) ;
#10054=ORIENTED_EDGE ( 'NONE', *, *, #40089, .T. ) ;
#10410=( NAMED_UNIT ( * ) SI_UNIT ( $, .STERADIAN. ) SOLID_ANGLE_UNIT ( ) );
#10670=EDGE_CURVE ( 'NONE', #3869, #70831, #100369, .T. ) ;
#10728=AXIS2_PLACEMENT_3D ( 'NONE', #14983, #57033, #47878 ) ;
#11087=CARTESIAN_POINT ( 'NONE',  ( 121.1901574356003550, 4.501353321498349658, -60.59507871780015620 ) ) ;
#11463=CARTESIAN_POINT ( 'NONE',  ( -0.000000000000000000, 58.72416816948006613, -16.91618513671782509 ) ) ;
#11627=CARTESIAN_POINT ( 'NONE',  ( 3.200388772515927248E-15, 60.33964880548970200, -13.06657876680918662 ) ) ;
#11822=MECHANICAL_DESIGN_GEOMETRIC_PRESENTATION_REPRESENTATION('',(#97909),#101384);
#12163=CARTESIAN_POINT ( 'NONE',  ( 1.458152649223318708E-14, 7.666536031838887766, -59.53359981990485750 ) ) ;
#12205=PRODUCT ( '12. Movable Jaw', '12. Movable Jaw', '', ( #31506 ) ) ;
#12212=( NAMED_UNIT ( * ) PLANE_ANGLE_UNIT ( ) SI_UNIT ( $, .RADIAN. ) );
#12507=UNCERTAINTY_MEASURE_WITH_UNIT (LENGTH_MEASURE( 1.000000000000000082E-05 ), #70906, 'distance_accuracy_value', 'NONE');
#12526=CARTESIAN_POINT ( 'NONE',  ( -1.600194386257964019E-15, 60.33964880548970200, 13.06657876680918662 ) ) ;
#12689=CARTESIAN_POINT ( 'NONE',  ( 39.18206537991729022, 57.18445727710330573, 19.59103268995865221 ) ) ;
#12695=( NAMED_UNIT ( * ) SI_UNIT ( $, .STERADIAN. ) SOLID_ANGLE_UNIT ( ) );
#13053=CARTESIAN_POINT ( 'NONE',  ( -0.000000000000000000, 4.501353321498349658, -60.59507871780017751 ) ) ;
#13219=CARTESIAN_POINT ( 'NONE',  ( -6.738183602098732403E-15, 17.51648154115788714, 55.02144460582525909 ) ) ;
#13226=SURFACE_SIDE_STYLE ('',( #52624 ) ) ;
#13237=CARTESIAN_POINT ( 'NONE',  ( 0.000000000000000000, 1.500000000000000444, -61.23540616453487218 ) ) ;
#13296=FILL_AREA_STYLE_COLOUR ( '', #52761 ) ;
#13754=EDGE_LOOP ( 'NONE', ( #101563, #57280, #100630, #89491 ) ) ;
#13756=CARTESIAN_POINT ( 'NONE',  ( 47.33333333333331439, 59.99999999999999289, -23.66666666666664653 ) ) ;
#13800=( NAMED_UNIT ( * ) SI_UNIT ( $, .STERADIAN. ) SOLID_ANGLE_UNIT ( ) );
#13949=( GEOMETRIC_REPRESENTATION_CONTEXT ( 3 ) GLOBAL_UNCERTAINTY_ASSIGNED_CONTEXT ( ( #33263 ) ) GLOBAL_UNIT_ASSIGNED_CONTEXT ( ( #48945, #16599, #96990 ) ) REPRESENTATION_CONTEXT ( 'NONE', 'WORKASPACE' ) );
#14240=CARTESIAN_POINT ( 'NONE',  ( -13.99999999999998046, 59.99999999999999289, -6.999999999999994671 ) ) ;
#14478=FILL_AREA_STYLE ('',( #15559 ) ) ;
#14632=EDGE_CURVE ( 'NONE', #6036, #23078, #40648, .T. ) ;
#14736=SURFACE_SIDE_STYLE ('',( #55714 ) ) ;
#14983=CARTESIAN_POINT ( 'NONE',  ( 0.000000000000000000, 0.000000000000000000, 0.000000000000000000 ) ) ;
#15361=( NAMED_UNIT ( * ) SI_UNIT ( $, .STERADIAN. ) SOLID_ANGLE_UNIT ( ) );
#15559=FILL_AREA_STYLE_COLOUR ( '', #36562 ) ;
#15588=CARTESIAN_POINT ( 'NONE',  ( -0.000000000000000000, 34.25047185182970111, -44.13186320217320713 ) ) ;
#16039=EDGE_LOOP ( 'NONE', ( #73498, #36751 ) ) ;
#16044=SURFACE_STYLE_USAGE ( .BOTH. , #47868 ) ;
#16062=CARTESIAN_POINT ( 'NONE',  ( 0.000000000000000000, 1.500000000000000000, -60.00000000000000000 ) ) ;
#16379=EDGE_CURVE ( 'NONE', #21078, #62090, #19655, .T. ) ;
#16390=COLOUR_RGB ( '', 0.31764706, 0.68627451, 0.89019608) ;
#16540=CARTESIAN_POINT ( 'NONE',  ( 18.71440884245025060, 61.34242035161803841, 9.357204421225128854 ) ) ;
#16599=( NAMED_UNIT ( * ) PLANE_ANGLE_UNIT ( ) SI_UNIT ( $, .RADIAN. ) );
#16810=ORIENTED_EDGE ( 'NONE', *, *, #57377, .T. ) ;
#17645=ORIENTED_EDGE ( 'NONE', *, *, #10670, .T. ) ;
#17882=CIRCLE ( 'NONE', #86796, 60.00000000000000000 ) ;
#18157=CARTESIAN_POINT ( 'NONE',  ( 13.99999999999998401, 61.49999999999999289, -6.999999999999989342 ) ) ;
#18191=EDGE_LOOP ( 'NONE', ( #104893, #69116 ) ) ;
#18374=DIRECTION ( 'NONE',  ( 0.000000000000000000, 1.000000000000000000, 0.000000000000000000 ) ) ;
#18537=CARTESIAN_POINT ( 'NONE',  ( -16.32074838266548156, 61.49999999999999289, -8.160374191332742555 ) ) ;
#18628=CARTESIAN_POINT ( 'NONE',  ( -6.851679529983103610E-15, 22.97884757028485225, 55.94820918777160301 ) ) ;
#19059=ADVANCED_BREP_SHAPE_REPRESENTATION ( '', ( #51736, #10728 ), #21183 ) ;
#19264=CARTESIAN_POINT ( 'NONE',  ( -6.011841252072294266E-15, 27.55047179872464724, 49.09040922050319011 ) ) ;
#19597=ADVANCED_FACE ( 'NONE', ( #95871 ), #104474, .F. ) ;
#19628=CARTESIAN_POINT ( 'NONE',  ( -33.83237027343564307, 58.72416816948007323, 16.91618513671782154 ) ) ;
#19655=CIRCLE ( 'NONE', #78183, 6.999999999999992895 ) ;
#19786=CARTESIAN_POINT ( 'NONE',  ( 6.819038153627915297E-15, 51.11204936430951307, -27.84083606136722366 ) ) ;
#20107=DIRECTION ( 'NONE',  ( 0.000000000000000000, 1.000000000000000000, 0.000000000000000000 ) ) ;
#20554=ADVANCED_FACE ( 'NONE', ( #88731 ), #103842, .F. ) ;
#20575=CARTESIAN_POINT ( 'NONE',  ( -3.068228200247434202E-15, 53.37899725327129374, 25.05398456423234066 ) ) ;
#20701=CARTESIAN_POINT ( 'NONE',  ( -13.99999999999998046, 61.49999999999999289, -6.999999999999992895 ) ) ;
#20860=CARTESIAN_POINT ( 'NONE',  ( -2.399209547574901823E-15, 57.18445727710329862, 19.59103268995865221 ) ) ;
#20927=CARTESIAN_POINT ( 'NONE',  ( 7.592810154713590230E-15, 1.500000000000000000, -62.00000000000000000 ) ) ;
#21078=VERTEX_POINT ( 'NONE', #85290 ) ;
#21183=( GEOMETRIC_REPRESENTATION_CONTEXT ( 3 ) GLOBAL_UNCERTAINTY_ASSIGNED_CONTEXT ( ( #100320 ) ) GLOBAL_UNIT_ASSIGNED_CONTEXT ( ( #34411, #5718, #28441 ) ) REPRESENTATION_CONTEXT ( 'NONE', 'WORKASPACE' ) );
#21209=CARTESIAN_POINT ( 'NONE',  ( -98.18081844100633759, 27.55047179872464724, 49.09040922050316880 ) ) ;
#21363=CARTESIAN_POINT ( 'NONE',  ( -1.446302031375384789E-15, 60.76237703744687479, 11.80995232570204045 ) ) ;
#21378=CARTESIAN_POINT ( 'NONE',  ( 0.000000000000000000, 51.11204936430951307, -27.84083606136722366 ) ) ;
#21567=EDGE_CURVE ( 'NONE', #23946, #25901, #59170, .T. ) ;
#21598=ADVANCED_FACE ( 'NONE', ( #81821 ), #65667, .T. ) ;
#21898=CARTESIAN_POINT ( 'NONE',  ( -2.898330757982067934E-15, 60.00000000000000000, 23.66666666666665719 ) ) ;
#21910=ORIENTED_EDGE ( 'NONE', *, *, #16379, .F. ) ;
#21966=DIRECTION ( 'NONE',  ( 0.000000000000000000, 1.000000000000000000, 0.000000000000000000 ) ) ;
#22237=UNCERTAINTY_MEASURE_WITH_UNIT (LENGTH_MEASURE( 1.000000000000000082E-05 ), #98513, 'distance_accuracy_value', 'NONE');
#22353=ADVANCED_FACE ( 'NONE', ( #37024 ), #98993, .F. ) ;
#22537=CARTESIAN_POINT ( 'NONE',  ( 0.000000000000000000, 60.00000000000000000, 0.000000000000000000 ) ) ;
#22603=UNCERTAINTY_MEASURE_WITH_UNIT (LENGTH_MEASURE( 1.000000000000000082E-05 ), #87873, 'distance_accuracy_value', 'NONE');
#22635=( NAMED_UNIT ( * ) SI_UNIT ( $, .STERADIAN. ) SOLID_ANGLE_UNIT ( ) );
#22696=COLOUR_RGB ( '', 0.09019608, 0.27058824, 0.51372549) ;
#23078=VERTEX_POINT ( 'NONE', #38475 ) ;
#23091=ORIENTED_EDGE ( 'NONE', *, *, #16379, .T. ) ;
#23154=( NAMED_UNIT ( * ) PLANE_ANGLE_UNIT ( ) SI_UNIT ( $, .RADIAN. ) );
#23271=MECHANICAL_DESIGN_GEOMETRIC_PRESENTATION_REPRESENTATION('',(#71512),#85224);
#23443=CARTESIAN_POINT ( 'NONE',  ( -5.796661515964135868E-15, 60.00000000000000000, 23.66666666666665719 ) ) ;
#23590=SURFACE_STYLE_FILL_AREA ( #30084 ) ;
#23657=FACE_BOUND ( 'NONE', #52533, .T. ) ;
#23716=CARTESIAN_POINT ( 'NONE',  ( -122.4708123290697159, 1.499999999999992450, -61.23540616453487218 ) ) ;
#23946=VERTEX_POINT ( 'NONE', #52519 ) ;
#23949=FILL_AREA_STYLE_COLOUR ( '', #64635 ) ;
#23984=CARTESIAN_POINT ( 'NONE',  ( -1.469576158976823671E-14, 0.000000000000000000, 60.00000000000000000 ) ) ;
#24012=CIRCLE ( 'NONE', #30942, 60.00000000000000000 ) ;
#24253=CARTESIAN_POINT ( 'NONE',  ( -121.1901574356003408, 4.501353321498349658, -60.59507871780017751 ) ) ;
#24369=B_SPLINE_CURVE_WITH_KNOTS ( 'NONE', 3,
 ( #51399, #27173, #75134, #2308, #78209, #50333, #49810, #20575, #70121, #62060, #94949, #82715, #8819, #41723, #33652, #66532, #99405, #58446 ),
 .UNSPECIFIED., .F., .F.,
 ( 4, 2, 2, 2, 2, 2, 2, 2, 4 ),
 ( 0.000000000000000000, 0.06143467464390223176, 0.1228693492878044635, 0.2457386985756090381, 0.3686080478634136126, 0.4914773971512180761, 0.7372160957268271142, 0.8600854450146315777, 0.9829547943024361523 ),
 .UNSPECIFIED. ) ;
#24660=CARTESIAN_POINT ( 'NONE',  ( 16.32074838266548511, 61.49999999999999289, -8.160374191332739002 ) ) ;
#24994=PRESENTATION_STYLE_ASSIGNMENT (( #64898 ) ) ;
#25197=CARTESIAN_POINT ( 'NONE',  ( -8.572527594031464315E-16, 61.50000000000000000, 6.999999999999992895 ) ) ;
#25901=VERTEX_POINT ( 'NONE', #105125 ) ;
#26278=CARTESIAN_POINT ( 'NONE',  ( 1.714505518806292863E-15, 61.50000000000000000, -6.999999999999992895 ) ) ;
#26468=MECHANICAL_DESIGN_GEOMETRIC_PRESENTATION_REPRESENTATION('',(#79771),#93578);
#26674=EDGE_CURVE ( 'NONE', #62090, #70831, #24369, .T. ) ;
#27014=DIRECTION ( 'NONE',  ( 0.000000000000000000, 0.000000000000000000, 1.000000000000000000 ) ) ;
#27173=CARTESIAN_POINT ( 'NONE',  ( -9.993576133260312108E-16, 61.49999999999999289, 8.160374191332742555 ) ) ;
#27211=PRODUCT_DEFINITION ( 'UNKNOWN', '', #88740, #92021 ) ;
#27347=CARTESIAN_POINT ( 'NONE',  ( 1.389906337552808880E-14, 14.17434517210798184, -56.74723269274520021 ) ) ;
#27616=UNCERTAINTY_MEASURE_WITH_UNIT (LENGTH_MEASURE( 1.000000000000000082E-05 ), #65958, 'distance_accuracy_value', 'NONE');
#27882=CARTESIAN_POINT ( 'NONE',  ( 1.484151383916717602E-14, 4.501353321498349658, -60.59507871780017751 ) ) ;
#28039=COLOUR_RGB ( '', 0.40784314, 0.44705882, 0.49803922) ;
#28239=( NAMED_UNIT ( * ) PLANE_ANGLE_UNIT ( ) SI_UNIT ( $, .RADIAN. ) );
#28353=ADVANCED_FACE ( 'NONE', ( #37101, #79633 ), #87216, .F. ) ;
#28396=CARTESIAN_POINT ( 'NONE',  ( 122.4708123290697444, 1.499999999999992450, -61.23540616453485086 ) ) ;
#28401=SURFACE_STYLE_USAGE ( .BOTH. , #13226 ) ;
#28441=( NAMED_UNIT ( * ) SI_UNIT ( $, .STERADIAN. ) SOLID_ANGLE_UNIT ( ) );
#28944=CARTESIAN_POINT ( 'NONE',  ( 26.13315753361836613, 60.33964880548970910, -13.06657876680917774 ) ) ;
#28950=( NAMED_UNIT ( * ) PLANE_ANGLE_UNIT ( ) SI_UNIT ( $, .RADIAN. ) );
#29276=DIRECTION ( 'NONE',  ( 0.000000000000000000, 1.000000000000000000, 0.000000000000000000 ) ) ;
#29466=CARTESIAN_POINT ( 'NONE',  ( 26.13315753361836613, 60.33964880548970910, 13.06657876680918839 ) ) ;
#29471=CARTESIAN_POINT ( 'NONE',  ( 1.469576158976823671E-14, 0.000000000000000000, -60.00000000000000000 ) ) ;
#29541=FILL_AREA_STYLE ('',( #13296 ) ) ;
#29692=CARTESIAN_POINT ( 'NONE',  ( 0.000000000000000000, 0.000000000000000000, -60.00000000000000000 ) ) ;
#29824=CARTESIAN_POINT ( 'NONE',  ( -7.420756919583589587E-15, 4.501353321498349658, 60.59507871780017751 ) ) ;
#29939=( NAMED_UNIT ( * ) PLANE_ANGLE_UNIT ( ) SI_UNIT ( $, .RADIAN. ) );
#30026=SURFACE_SIDE_STYLE ('',( #45663 ) ) ;
#30084=FILL_AREA_STYLE ('',( #80190 ) ) ;
#30733=AXIS2_PLACEMENT_3D ( 'NONE', #100615, #90950, #92523 ) ;
#30884=AXIS2_PLACEMENT_3D ( 'NONE', #78285, #20107, #95027 ) ;
#30942=AXIS2_PLACEMENT_3D ( 'NONE', #7035, #64755, #9150 ) ;
#31011=CARTESIAN_POINT ( 'NONE',  ( 2.898330757982067934E-15, 60.00000000000000000, -23.66666666666665719 ) ) ;
#31068=CARTESIAN_POINT ( 'NONE',  ( -0.000000000000000000, 60.76237703744687479, -11.80995232570204045 ) ) ;
#31378=LINE ( 'NONE', #55068, #43170 ) ;
#31506=PRODUCT_CONTEXT ( 'NONE', #89333, 'mechanical' ) ;
#31537=FACE_OUTER_BOUND ( 'NONE', #83926, .T. ) ;
#31743=SURFACE_SIDE_STYLE ('',( #105602 ) ) ;
#31796=CARTESIAN_POINT ( 'NONE',  ( -6.949531687764044400E-15, 14.17434517210798184, 56.74723269274520021 ) ) ;
#32041=SURFACE_STYLE_USAGE ( .BOTH. , #38159 ) ;
#32098=SURFACE_STYLE_FILL_AREA ( #55793 ) ;
#32810=FACE_OUTER_BOUND ( 'NONE', #16039, .T. ) ;
#32868=CARTESIAN_POINT ( 'NONE',  ( -119.0671996398097008, 7.666536031838888654, 59.53359981990485039 ) ) ;
#33058=DIRECTION ( 'NONE',  ( 0.000000000000000000, 0.000000000000000000, 1.000000000000000000 ) ) ;
#33070=ORIENTED_EDGE ( 'NONE', *, *, #21567, .T. ) ;
#33263=UNCERTAINTY_MEASURE_WITH_UNIT (LENGTH_MEASURE( 1.000000000000000082E-05 ), #48945, 'distance_accuracy_value', 'NONE');
#33456=CARTESIAN_POINT ( 'NONE',  ( 0.000000000000000000, 61.50000000000000000, 0.000000000000000000 ) ) ;
#33643=CARTESIAN_POINT ( 'NONE',  ( -47.33333333333330728, 59.99999999999999289, -23.66666666666666785 ) ) ;
#33652=CARTESIAN_POINT ( 'NONE',  ( -6.949531687764044400E-15, 14.17434517210798184, 56.74723269274520021 ) ) ;
#33815=FILL_AREA_STYLE ('',( #91508 ) ) ;
#34411=( LENGTH_UNIT ( ) NAMED_UNIT ( * ) SI_UNIT ( .MILLI., .METRE. ) );
#35009=COLOUR_RGB ( '', 0.08235294, 0.09019608, 0.10196078) ;
#35257=SURFACE_SIDE_STYLE ('',( #2310 ) ) ;
#35324=CARTESIAN_POINT ( 'NONE',  ( 0.000000000000000000, 0.000000000000000000, 0.000000000000000000 ) ) ;
#35420=CARTESIAN_POINT ( 'NONE',  ( 113.4944653854903720, 14.17434517210798006, 56.74723269274521442 ) ) ;
#35435=ORIENTED_EDGE ( 'NONE', *, *, #72140, .F. ) ;
#35966=CARTESIAN_POINT ( 'NONE',  ( 8.176795461013406112E-15, 46.03420836107012093, -33.38430095398285147 ) ) ;
#36339=CARTESIAN_POINT ( 'NONE',  ( -8.572527594031464315E-16, 61.50000000000000000, 6.999999999999992895 ) ) ;
#36423=COLOUR_RGB ( '', 0.40784314, 0.44705882, 0.49803922) ;
#36497=CARTESIAN_POINT ( 'NONE',  ( 110.0428892116504755, 17.51648154115788358, 55.02144460582527330 ) ) ;
#36562=COLOUR_RGB ( '', 0.40784314, 0.44705882, 0.49803922) ;
#36751=ORIENTED_EDGE ( 'NONE', *, *, #72140, .T. ) ;
#36830=CARTESIAN_POINT ( 'NONE',  ( 0.000000000000000000, 61.50000000000000000, 0.000000000000000000 ) ) ;
#37018=CARTESIAN_POINT ( 'NONE',  ( -3.068228200247434202E-15, 53.37899725327129374, 25.05398456423234066 ) ) ;
#37024=FACE_OUTER_BOUND ( 'NONE', #13754, .T. ) ;
#37080=B_SPLINE_CURVE_WITH_KNOTS ( 'NONE', 3,
 ( #64470, #38611, #104928, #31068, #105958, #62355, #104373, #47197, #21378, #39139, #63946, #6743, #46161, #54215, #87156, #96832, #39665, #13237 ),
 .UNSPECIFIED., .F., .F.,
 ( 4, 2, 2, 2, 2, 2, 2, 2, 4 ),
 ( 0.000000000000000000, 0.06143467464390223176, 0.1228693492878044635, 0.2457386985756090381, 0.3686080478634136126, 0.4914773971512180761, 0.7372160957268271142, 0.8600854450146315777, 0.9829547943024361523 ),
 .UNSPECIFIED. ) ;
#37101=FACE_OUTER_BOUND ( 'NONE', #55026, .T. ) ;
#37394=CARTESIAN_POINT ( 'NONE',  ( -39.18206537991729022, 57.18445727710330573, 19.59103268995864511 ) ) ;
#37554=CARTESIAN_POINT ( 'NONE',  ( 66.76860190796567451, 46.03420836107012093, 33.38430095398285857 ) ) ;
#37561=CARTESIAN_POINT ( 'NONE',  ( 13.99999999999998401, 59.99999999999999289, -6.999999999999989342 ) ) ;
#37761=SURFACE_STYLE_USAGE ( .BOTH. , #38282 ) ;
#37923=CARTESIAN_POINT ( 'NONE',  ( -4.425930005958663723E-15, 43.22324503868515677, 36.14046114390016839 ) ) ;
#38089=CARTESIAN_POINT ( 'NONE',  ( 111.8964183755431918, 22.97884757028484870, 55.94820918777161722 ) ) ;
#38159=SURFACE_SIDE_STYLE ('',( #97806 ) ) ;
#38280=ORIENTED_EDGE ( 'NONE', *, *, #42042, .T. ) ;
#38282=SURFACE_SIDE_STYLE ('',( #38793 ) ) ;
#38475=CARTESIAN_POINT ( 'NONE',  ( 0.000000000000000000, 60.00000000000000000, 6.999999999999992895 ) ) ;
#38514=B_SPLINE_CURVE_WITH_KNOTS ( 'NONE', 3,
 ( #3537, #61796, #67736, #53152 ),
 .UNSPECIFIED., .F., .F.,
 ( 4, 4 ),
 ( 0.000000000000000000, 1.000000000000000000 ),
 .UNSPECIFIED. ) ;
#38604=( NAMED_UNIT ( * ) PLANE_ANGLE_UNIT ( ) SI_UNIT ( $, .RADIAN. ) );
#38611=CARTESIAN_POINT ( 'NONE',  ( -0.000000000000000000, 61.49999999999999289, -8.160374191332742555 ) ) ;
#38793=SURFACE_STYLE_FILL_AREA ( #14478 ) ;
#38849=AXIS2_PLACEMENT_3D ( 'NONE', #57318, #39581, #41158 ) ;
#38956=ORIENTED_EDGE ( 'NONE', *, *, #26674, .F. ) ;
#39134=CARTESIAN_POINT ( 'NONE',  ( 0.000000000000000000, 60.00000000000000000, 0.000000000000000000 ) ) ;
#39139=CARTESIAN_POINT ( 'NONE',  ( -0.000000000000000000, 46.03420836107012093, -33.38430095398285147 ) ) ;
#39235=DIRECTION ( 'NONE',  ( 0.000000000000000000, 1.000000000000000000, 0.000000000000000000 ) ) ;
#39581=DIRECTION ( 'NONE',  ( 0.000000000000000000, 1.000000000000000000, 0.000000000000000000 ) ) ;
#39661=PRESENTATION_STYLE_ASSIGNMENT (( #79568 ) ) ;
#39665=CARTESIAN_POINT ( 'NONE',  ( -0.000000000000000000, 4.501353321498349658, -60.59507871780017751 ) ) ;
#39880=CARTESIAN_POINT ( 'NONE',  ( -113.4944653854903862, 14.17434517210798006, -56.74723269274520732 ) ) ;
#40089=EDGE_CURVE ( 'NONE', #25901, #63111, #45687, .T. ) ;
#40323=SURFACE_STYLE_FILL_AREA ( #352 ) ;
#40462=DIRECTION ( 'NONE',  ( 0.000000000000000000, 1.000000000000000000, 0.000000000000000000 ) ) ;
#40562=CARTESIAN_POINT ( 'NONE',  ( 0.000000000000000000, 61.50000000000000000, 6.999999999999992895 ) ) ;
#40640=CIRCLE ( 'NONE', #71658, 61.23540616453487218 ) ;
#40648=CIRCLE ( 'NONE', #59617, 6.999999999999992895 ) ;
#40850=( LENGTH_UNIT ( ) NAMED_UNIT ( * ) SI_UNIT ( .MILLI., .METRE. ) );
#40875=FILL_AREA_STYLE ('',( #96471 ) ) ;
#40900=EDGE_CURVE ( 'NONE', #25901, #23946, #61762, .T. ) ;
#40931=CARTESIAN_POINT ( 'NONE',  ( 0.000000000000000000, 43.22324503868515677, -36.14046114390016839 ) ) ;
#41158=DIRECTION ( 'NONE',  ( 0.000000000000000000, 0.000000000000000000, 1.000000000000000000 ) ) ;
#41411=ADVANCED_FACE ( 'NONE', ( #45460 ), #53654, .T. ) ;
#41460=CARTESIAN_POINT ( 'NONE',  ( -72.28092228780032258, 43.22324503868516388, 36.14046114390016129 ) ) ;
#41723=CARTESIAN_POINT ( 'NONE',  ( -6.738183602098732403E-15, 17.51648154115788714, 55.02144460582525909 ) ) ;
#42042=EDGE_CURVE ( 'NONE', #23078, #62090, #75162, .T. ) ;
#42132=CARTESIAN_POINT ( 'NONE',  ( 0.000000000000000000, 1.500000000000000888, 0.000000000000000000 ) ) ;
#42236=CARTESIAN_POINT ( 'NONE',  ( -1.370335905996620722E-14, 22.97884757028485225, 55.94820918777160301 ) ) ;
#42871=CARTESIAN_POINT ( 'NONE',  ( 0.000000000000000000, 60.00000000000000000, 6.999999999999992895 ) ) ;
#43170=VECTOR ( 'NONE', #79358, 1000.000000000000000 ) ;
#43324=CARTESIAN_POINT ( 'NONE',  ( 0.000000000000000000, 61.34242035161803841, -9.357204421225127078 ) ) ;
#43484=CARTESIAN_POINT ( 'NONE',  ( 16.32074838266548156, 61.49999999999999289, 8.160374191332744331 ) ) ;
#43683=CARTESIAN_POINT ( 'NONE',  ( 0.000000000000000000, 60.00000000000000000, 0.000000000000000000 ) ) ;
#43847=FILL_AREA_STYLE_COLOUR ( '', #58341 ) ;
#43885=STYLED_ITEM ( 'NONE', ( #87106 ), #55887 ) ;
#44013=CARTESIAN_POINT ( 'NONE',  ( 98.18081844100633759, 27.55047179872464724, 49.09040922050319722 ) ) ;
#44390=CARTESIAN_POINT ( 'NONE',  ( -16.32074838266548156, 61.49999999999999289, 8.160374191332740779 ) ) ;
#44557=CARTESIAN_POINT ( 'NONE',  ( 122.4708123290697017, 1.499999999999992450, 61.23540616453489349 ) ) ;
#44732=CARTESIAN_POINT ( 'NONE',  ( 0.000000000000000000, 1.500000000000000000, 0.000000000000000000 ) ) ;
#44790=CARTESIAN_POINT ( 'NONE',  ( 0.000000000000000000, 1.500000000000000444, -61.23540616453487218 ) ) ;
#44813=EDGE_LOOP ( 'NONE', ( #78664, #50121, #38280, #76287 ) ) ;
#44935=SURFACE_STYLE_USAGE ( .BOTH. , #35257 ) ;
#45089=VERTEX_POINT ( 'NONE', #88942 ) ;
#45091=( GEOMETRIC_REPRESENTATION_CONTEXT ( 3 ) GLOBAL_UNCERTAINTY_ASSIGNED_CONTEXT ( ( #99049 ) ) GLOBAL_UNIT_ASSIGNED_CONTEXT ( ( #6295, #62969, #54850 ) ) REPRESENTATION_CONTEXT ( 'NONE', 'WORKASPACE' ) );
#45094=CARTESIAN_POINT ( 'NONE',  ( 72.28092228780032258, 43.22324503868516388, 36.14046114390017550 ) ) ;
#45460=FACE_OUTER_BOUND ( 'NONE', #62415, .T. ) ;
#45518=ORIENTED_EDGE ( 'NONE', *, *, #68620, .F. ) ;
#45583=SURFACE_STYLE_USAGE ( .BOTH. , #96262 ) ;
#45621=CARTESIAN_POINT ( 'NONE',  ( 88.26372640434641426, 34.25047185182970111, 44.13186320217322844 ) ) ;
#45625=CARTESIAN_POINT ( 'NONE',  ( -8.572527594031464315E-16, 60.00000000000000000, 6.999999999999992895 ) ) ;
#45663=SURFACE_STYLE_FILL_AREA ( #69413 ) ;
#45687=LINE ( 'NONE', #78048, #101393 ) ;
#45739=ORIENTED_EDGE ( 'NONE', *, *, #40900, .T. ) ;
#45985=CARTESIAN_POINT ( 'NONE',  ( -55.68167212273443312, 51.11204936430952017, -27.84083606136722011 ) ) ;
#46161=CARTESIAN_POINT ( 'NONE',  ( 0.000000000000000000, 27.55047179872464724, -49.09040922050319011 ) ) ;
#47197=CARTESIAN_POINT ( 'NONE',  ( -0.000000000000000000, 53.37899725327129374, -25.05398456423234066 ) ) ;
#47249=MECHANICAL_DESIGN_GEOMETRIC_PRESENTATION_REPRESENTATION('',(#61063),#95453);
#47868=SURFACE_SIDE_STYLE ('',( #40323 ) ) ;
#47878=DIRECTION ( 'NONE',  ( 1.000000000000000000, 0.000000000000000000, 0.000000000000000000 ) ) ;
#47942=CARTESIAN_POINT ( 'NONE',  ( -110.0428892116504755, 17.51648154115788358, -55.02144460582525198 ) ) ;
#48066=ORIENTED_EDGE ( 'NONE', *, *, #14632, .F. ) ;
#48429=AXIS2_PLACEMENT_3D ( 'NONE', #44732, #52262, #69532 ) ;
#48479=CARTESIAN_POINT ( 'NONE',  ( -0.000000000000000000, 46.03420836107012093, -33.38430095398285147 ) ) ;
#48924=PRESENTATION_STYLE_ASSIGNMENT (( #16044 ) ) ;
#48945=( LENGTH_UNIT ( ) NAMED_UNIT ( * ) SI_UNIT ( .MILLI., .METRE. ) );
#49004=CARTESIAN_POINT ( 'NONE',  ( -122.4708123290697444, 1.499999999999992450, 61.23540616453485796 ) ) ;
#49276=ORIENTED_EDGE ( 'NONE', *, *, #40089, .F. ) ;
#49429=SURFACE_SIDE_STYLE ('',( #49964 ) ) ;
#49810=CARTESIAN_POINT ( 'NONE',  ( -2.399209547574901823E-15, 57.18445727710329862, 19.59103268995865221 ) ) ;
#49964=SURFACE_STYLE_FILL_AREA ( #33815 ) ;
#50007=( NAMED_UNIT ( * ) SI_UNIT ( $, .STERADIAN. ) SOLID_ANGLE_UNIT ( ) );
#50121=ORIENTED_EDGE ( 'NONE', *, *, #90337, .F. ) ;
#50305=DIRECTION ( 'NONE',  ( 0.000000000000000000, 1.000000000000000000, 0.000000000000000000 ) ) ;
#50333=CARTESIAN_POINT ( 'NONE',  ( -2.071635198146551927E-15, 58.72416816948006613, 16.91618513671782509 ) ) ;
#50354=DIRECTION ( 'NONE',  ( 0.000000000000000000, 1.000000000000000000, 0.000000000000000000 ) ) ;
#51016=FACE_OUTER_BOUND ( 'NONE', #92169, .T. ) ;
#51399=CARTESIAN_POINT ( 'NONE',  ( 0.000000000000000000, 61.50000000000000000, 6.999999999999992895 ) ) ;
#51487=CARTESIAN_POINT ( 'NONE',  ( -7.347880794884119933E-15, 0.000000000000000000, 60.00000000000000000 ) ) ;
#51736=MANIFOLD_SOLID_BREP ( 'Thicken1', #53176 ) ;
#51930=CARTESIAN_POINT ( 'NONE',  ( -18.71440884245025060, 61.34242035161803841, -9.357204421225127078 ) ) ;
#52093=CARTESIAN_POINT ( 'NONE',  ( 121.1901574356003124, 4.501353321498349658, 60.59507871780019883 ) ) ;
#52262=DIRECTION ( 'NONE',  ( 0.000000000000000000, 1.000000000000000000, 0.000000000000000000 ) ) ;
#52461=CARTESIAN_POINT ( 'NONE',  ( 0.000000000000000000, 57.18445727710329862, -19.59103268995865221 ) ) ;
#52519=CARTESIAN_POINT ( 'NONE',  ( 7.592810154713590230E-15, 0.000000000000000000, -62.00000000000000000 ) ) ;
#52533=EDGE_LOOP ( 'NONE', ( #82004, #102124 ) ) ;
#52619=CARTESIAN_POINT ( 'NONE',  ( 33.83237027343564307, 58.72416816948007323, 16.91618513671782509 ) ) ;
#52624=SURFACE_STYLE_FILL_AREA ( #102250 ) ;
#52761=COLOUR_RGB ( '', 0.31764706, 0.68627451, 0.89019608) ;
#52910=EDGE_CURVE ( 'NONE', #6036, #70572, #38514, .T. ) ;
#53152=CARTESIAN_POINT ( 'NONE',  ( 0.000000000000000000, 0.000000000000000000, -60.00000000000000000 ) ) ;
#53176=CLOSED_SHELL ( 'NONE', ( #55887, #61803, #20554, #99188, #21598, #19597, #41411, #73760, #22353, #28353 ) ) ;
#53654=( BOUNDED_SURFACE ( )  B_SPLINE_SURFACE ( 3, 3, ( 
 ( #61660, #20701, #101020, #36339 ),
 ( #85932, #18537, #44390, #77819 ),
 ( #43324, #51930, #76737, #86468 ),
 ( #69209, #102077, #68679, #101560 ),
 ( #3929, #60590, #93479, #12526 ),
 ( #11463, #78334, #19628, #59517 ),
 ( #52461, #4451, #37394, #105659 ),
 ( #6962, #4992, #80850, #56568 ),
 ( #78864, #45985, #70784, #54039 ),
 ( #48479, #89493, #82454, #8021 ),
 ( #40931, #65745, #41460, #37923 ),
 ( #15588, #81371, #73824, #62191 ),
 ( #95076, #97556, #21209, #106719 ),
 ( #81905, #47942, #65207, #103679 ),
 ( #7481, #39880, #98102, #31796 ),
 ( #72753, #86984, #32868, #64684 ),
 ( #13053, #24253, #97039, #29824 ),
 ( #88959, #23716, #49004, #73280 ) ),
 .UNSPECIFIED., .F., .F., .F. ) 
 B_SPLINE_SURFACE_WITH_KNOTS ( ( 4, 2, 2, 2, 2, 2, 2, 2, 4 ),
 ( 4, 4 ),
 ( 0.000000000000000000, 0.06249999999999997224, 0.1249999999999999445, 0.2500000000000000000, 0.3750000000000000555, 0.5000000000000000000, 0.7500000000000000000, 0.8750000000000000000, 1.000000000000000000 ),
 ( 0.000000000000000000, 1.000000000000000000 ),
 .UNSPECIFIED. ) 
 GEOMETRIC_REPRESENTATION_ITEM ( )  RATIONAL_B_SPLINE_SURFACE ( (
 ( 1.000000000000000000, 0.3333333333333334259, 0.3333333333333334259, 1.000000000000000000),
 ( 1.000000000000000000, 0.3333333333333334259, 0.3333333333333334259, 1.000000000000000000),
 ( 1.000000000000000000, 0.3333333333333334259, 0.3333333333333334259, 1.000000000000000000),
 ( 1.000000000000000000, 0.3333333333333334259, 0.3333333333333334259, 1.000000000000000000),
 ( 1.000000000000000000, 0.3333333333333334259, 0.3333333333333334259, 1.000000000000000000),
 ( 1.000000000000000000, 0.3333333333333334259, 0.3333333333333334259, 1.000000000000000000),
 ( 1.000000000000000000, 0.3333333333333334259, 0.3333333333333334259, 1.000000000000000000),
 ( 1.000000000000000000, 0.3333333333333334259, 0.3333333333333334259, 1.000000000000000000),
 ( 1.000000000000000000, 0.3333333333333334259, 0.3333333333333334259, 1.000000000000000000),
 ( 1.000000000000000000, 0.3333333333333334259, 0.3333333333333334259, 1.000000000000000000),
 ( 1.000000000000000000, 0.3333333333333334259, 0.3333333333333334259, 1.000000000000000000),
 ( 1.000000000000000000, 0.3333333333333334259, 0.3333333333333334259, 1.000000000000000000),
 ( 1.000000000000000000, 0.3333333333333334259, 0.3333333333333334259, 1.000000000000000000),
 ( 1.000000000000000000, 0.3333333333333334259, 0.3333333333333334259, 1.000000000000000000),
 ( 1.000000000000000000, 0.3333333333333334259, 0.3333333333333334259, 1.000000000000000000),
 ( 1.000000000000000000, 0.3333333333333334259, 0.3333333333333334259, 1.000000000000000000),
 ( 1.000000000000000000, 0.3333333333333334259, 0.3333333333333334259, 1.000000000000000000),
 ( 1.000000000000000000, 0.3333333333333334259, 0.3333333333333334259, 1.000000000000000000) ) ) 
 REPRESENTATION_ITEM ( '' )  SURFACE ( )  );
#53693=CARTESIAN_POINT ( 'NONE',  ( -2.071635198146551927E-15, 58.72416816948006613, 16.91618513671782509 ) ) ;
#53742=SHAPE_REPRESENTATION_RELATIONSHIP ( 'NONE' , 'NONE' ,  #59830, #19059 ) ;
#54008=EDGE_LOOP ( 'NONE', ( #45739, #92959, #105305, #49276 ) ) ;
#54039=CARTESIAN_POINT ( 'NONE',  ( -3.409519076813957649E-15, 51.11204936430951307, 27.84083606136722366 ) ) ;
#54203=CARTESIAN_POINT ( 'NONE',  ( -5.404594501095027787E-15, 34.25047185182970111, 44.13186320217320713 ) ) ;
#54215=CARTESIAN_POINT ( 'NONE',  ( -0.000000000000000000, 17.51648154115788714, -55.02144460582525909 ) ) ;
#54743=CARTESIAN_POINT ( 'NONE',  ( 5.796661515964135868E-15, 60.00000000000000000, -23.66666666666665719 ) ) ;
#54747=DIRECTION ( 'NONE',  ( 0.000000000000000000, 0.000000000000000000, 1.000000000000000000 ) ) ;
#54811=EDGE_CURVE ( 'NONE', #70572, #45089, #17882, .T. ) ;
#54850=( NAMED_UNIT ( * ) SI_UNIT ( $, .STERADIAN. ) SOLID_ANGLE_UNIT ( ) );
#55026=EDGE_LOOP ( 'NONE', ( #62782, #7062 ) ) ;
#55068=CARTESIAN_POINT ( 'NONE',  ( 8.572527594031464315E-16, 60.00000000000000000, -6.999999999999992895 ) ) ;
#55446=SURFACE_STYLE_USAGE ( .BOTH. , #31743 ) ;
#55714=SURFACE_STYLE_FILL_AREA ( #63855 ) ;
#55786=UNCERTAINTY_MEASURE_WITH_UNIT (LENGTH_MEASURE( 1.000000000000000082E-05 ), #40850, 'distance_accuracy_value', 'NONE');
#55793=FILL_AREA_STYLE ('',( #5681 ) ) ;
#55887=ADVANCED_FACE ( 'NONE', ( #31537 ), #67528, .F. ) ;
#56280=CARTESIAN_POINT ( 'NONE',  ( -47.33333333333331439, 59.99999999999999289, 23.66666666666664653 ) ) ;
#56437=SURFACE_STYLE_USAGE ( .BOTH. , #81245 ) ;
#56509=DIRECTION ( 'NONE',  ( 0.000000000000000000, -0.000000000000000000, 1.000000000000000000 ) ) ;
#56568=CARTESIAN_POINT ( 'NONE',  ( -3.068228200247433018E-15, 53.37899725327129374, 25.05398456423234066 ) ) ;
#56812=( NAMED_UNIT ( * ) PLANE_ANGLE_UNIT ( ) SI_UNIT ( $, .RADIAN. ) );
#56891=ORIENTED_EDGE ( 'NONE', *, *, #52910, .F. ) ;
#57016=EDGE_LOOP ( 'NONE', ( #45518, #33070, #10054, #35435 ) ) ;
#57023=FILL_AREA_STYLE_COLOUR ( '', #35009 ) ;
#57033=DIRECTION ( 'NONE',  ( 0.000000000000000000, 0.000000000000000000, 1.000000000000000000 ) ) ;
#57280=ORIENTED_EDGE ( 'NONE', *, *, #90337, .T. ) ;
#57318=CARTESIAN_POINT ( 'NONE',  ( 0.000000000000000000, 0.000000000000000000, 0.000000000000000000 ) ) ;
#57377=EDGE_CURVE ( 'NONE', #70831, #3869, #40640, .T. ) ;
#57513=CARTESIAN_POINT ( 'NONE',  ( 1.998715226652062816E-15, 61.49999999999999289, -8.160374191332742555 ) ) ;
#57549=DIRECTION ( 'NONE',  ( 0.000000000000000000, 0.000000000000000000, 1.000000000000000000 ) ) ;
#57884=CARTESIAN_POINT ( 'NONE',  ( -119.9999999999999432, 0.000000000000000000, -60.00000000000001421 ) ) ;
#57989=ORIENTED_EDGE ( 'NONE', *, *, #26674, .T. ) ;
#58341=COLOUR_RGB ( '', 0.08235294, 0.09019608, 0.10196078) ;
#58412=CARTESIAN_POINT ( 'NONE',  ( 7.592810154713590230E-15, 0.000000000000000000, -62.00000000000000000 ) ) ;
#58446=CARTESIAN_POINT ( 'NONE',  ( -7.499174415388573091E-15, 1.500000000000000444, 61.23540616453487218 ) ) ;
#59015=UNCERTAINTY_MEASURE_WITH_UNIT (LENGTH_MEASURE( 1.000000000000000082E-05 ), #89263, 'distance_accuracy_value', 'NONE');
#59170=CIRCLE ( 'NONE', #91867, 62.00000000000000000 ) ;
#59517=CARTESIAN_POINT ( 'NONE',  ( -2.071635198146551533E-15, 58.72416816948006613, 16.91618513671782509 ) ) ;
#59617=AXIS2_PLACEMENT_3D ( 'NONE', #43683, #18374, #27014 ) ;
#59830=SHAPE_REPRESENTATION ( '12. Movable Jaw', ( #10728 ), #21183 ) ;
#60225=CARTESIAN_POINT ( 'NONE',  ( 119.0671996398097008, 7.666536031838888654, -59.53359981990482908 ) ) ;
#60590=CARTESIAN_POINT ( 'NONE',  ( -26.13315753361836613, 60.33964880548970910, -13.06657876680918662 ) ) ;
#60716=AXIS2_PLACEMENT_3D ( 'NONE', #39134, #96308, #54747 ) ;
#60747=CARTESIAN_POINT ( 'NONE',  ( 8.851860011917325868E-15, 43.22324503868515677, -36.14046114390016839 ) ) ;
#60753=CARTESIAN_POINT ( 'NONE',  ( 119.9999999999999858, 0.000000000000000000, -59.99999999999997158 ) ) ;
#61063=STYLED_ITEM ( 'NONE', ( #8444 ), #61803 ) ;
#61148=( GEOMETRIC_REPRESENTATION_CONTEXT ( 3 ) GLOBAL_UNCERTAINTY_ASSIGNED_CONTEXT ( ( #12507 ) ) GLOBAL_UNIT_ASSIGNED_CONTEXT ( ( #70906, #29939, #104321 ) ) REPRESENTATION_CONTEXT ( 'NONE', 'WORKASPACE' ) );
#61269=CARTESIAN_POINT ( 'NONE',  ( 88.26372640434641426, 34.25047185182970111, -44.13186320217318581 ) ) ;
#61660=CARTESIAN_POINT ( 'NONE',  ( 0.000000000000000000, 61.50000000000000000, -6.999999999999992895 ) ) ;
#61762=CIRCLE ( 'NONE', #30733, 62.00000000000000000 ) ;
#61796=CARTESIAN_POINT ( 'NONE',  ( 0.000000000000000000, 60.00000000000000000, -23.66666666666665719 ) ) ;
#61803=ADVANCED_FACE ( 'NONE', ( #51016 ), #74429, .T. ) ;
#61818=CARTESIAN_POINT ( 'NONE',  ( 50.10796912846466000, 53.37899725327127953, 25.05398456423234776 ) ) ;
#62060=CARTESIAN_POINT ( 'NONE',  ( -4.088397730506703845E-15, 46.03420836107012093, 33.38430095398285147 ) ) ;
#62090=VERTEX_POINT ( 'NONE', #40562 ) ;
#62191=CARTESIAN_POINT ( 'NONE',  ( -5.404594501095028576E-15, 34.25047185182970111, 44.13186320217320713 ) ) ;
#62337=CARTESIAN_POINT ( 'NONE',  ( 50.10796912846467421, 53.37899725327127953, -25.05398456423232645 ) ) ;
#62355=CARTESIAN_POINT ( 'NONE',  ( -0.000000000000000000, 58.72416816948006613, -16.91618513671782509 ) ) ;
#62403=MECHANICAL_DESIGN_GEOMETRIC_PRESENTATION_REPRESENTATION('',(#67560),#105496);
#62415=EDGE_LOOP ( 'NONE', ( #38956, #21910, #98517, #17645 ) ) ;
#62782=ORIENTED_EDGE ( 'NONE', *, *, #40900, .F. ) ;
#62969=( NAMED_UNIT ( * ) PLANE_ANGLE_UNIT ( ) SI_UNIT ( $, .RADIAN. ) );
#63084=AXIS2_PLACEMENT_3D ( 'NONE', #4704, #21966, #103391 ) ;
#63111=VERTEX_POINT ( 'NONE', #2230 ) ;
#63855=FILL_AREA_STYLE ('',( #23949 ) ) ;
#63946=CARTESIAN_POINT ( 'NONE',  ( 0.000000000000000000, 43.22324503868515677, -36.14046114390016839 ) ) ;
#64045=EDGE_LOOP ( 'NONE', ( #48066, #677, #23091, #8361 ) ) ;
#64382=CYLINDRICAL_SURFACE ( 'NONE', #38849, 62.00000000000000000 ) ;
#64417=FILL_AREA_STYLE ('',( #5114 ) ) ;
#64465=SURFACE_SIDE_STYLE ('',( #32098 ) ) ;
#64470=CARTESIAN_POINT ( 'NONE',  ( 8.572527594031464315E-16, 61.50000000000000000, -6.999999999999992895 ) ) ;
#64635=COLOUR_RGB ( '', 0.66274510, 0.83137255, 0.94901961) ;
#64638=CARTESIAN_POINT ( 'NONE',  ( 8.572527594031464315E-16, 60.00000000000000000, -6.999999999999992895 ) ) ;
#64684=CARTESIAN_POINT ( 'NONE',  ( -7.290763246116593538E-15, 7.666536031838887766, 59.53359981990485750 ) ) ;
#64755=DIRECTION ( 'NONE',  ( 0.000000000000000000, 1.000000000000000000, 0.000000000000000000 ) ) ;
#64898=SURFACE_STYLE_USAGE ( .BOTH. , #14736 ) ;
#64915=LINE ( 'NONE', #58412, #87597 ) ;
#65207=CARTESIAN_POINT ( 'NONE',  ( -110.0428892116504755, 17.51648154115788358, 55.02144460582523777 ) ) ;
#65328=AXIS2_PLACEMENT_3D ( 'NONE', #36830, #29276, #102591 ) ;
#65436=SHAPE_DEFINITION_REPRESENTATION ( #86297, #59830 ) ;
#65667=CYLINDRICAL_SURFACE ( 'NONE', #84947, 62.00000000000000000 ) ;
#65745=CARTESIAN_POINT ( 'NONE',  ( -72.28092228780032258, 43.22324503868516388, -36.14046114390016839 ) ) ;
#65958=( LENGTH_UNIT ( ) NAMED_UNIT ( * ) SI_UNIT ( .MILLI., .METRE. ) );
#66151=CARTESIAN_POINT ( 'NONE',  ( 18.71440884245025416, 61.34242035161803841, -9.357204421225121749 ) ) ;
#66524=CARTESIAN_POINT ( 'NONE',  ( 7.347880794884118356E-15, 0.000000000000000000, -60.00000000000000000 ) ) ;
#66532=CARTESIAN_POINT ( 'NONE',  ( -7.290763246116595115E-15, 7.666536031838887766, 59.53359981990485750 ) ) ;
#66567=DIRECTION ( 'NONE',  ( 0.000000000000000000, 1.000000000000000000, 0.000000000000000000 ) ) ;
#67528=( BOUNDED_SURFACE ( )  B_SPLINE_SURFACE ( 3, 3, ( 
 ( #88157, #14240, #104868, #80040 ),
 ( #31011, #33643, #56280, #23443 ),
 ( #90270, #81103, #90809, #42236 ),
 ( #66524, #57884, #97821, #23984 ) ),
 .UNSPECIFIED., .F., .F., .F. ) 
 B_SPLINE_SURFACE_WITH_KNOTS ( ( 4, 4 ),
 ( 4, 4 ),
 ( 0.000000000000000000, 1.000000000000000000 ),
 ( 0.000000000000000000, 1.000000000000000000 ),
 .UNSPECIFIED. ) 
 GEOMETRIC_REPRESENTATION_ITEM ( )  RATIONAL_B_SPLINE_SURFACE ( (
 ( 1.000000000000000000, 0.3333333333333334259, 0.3333333333333334259, 1.000000000000000000),
 ( 1.000000000000000000, 0.3333333333333334259, 0.3333333333333334259, 1.000000000000000000),
 ( 1.000000000000000000, 0.3333333333333334259, 0.3333333333333334259, 1.000000000000000000),
 ( 1.000000000000000000, 0.3333333333333334259, 0.3333333333333334259, 1.000000000000000000) ) ) 
 REPRESENTATION_ITEM ( '' )  SURFACE ( )  );
#67554=MECHANICAL_DESIGN_GEOMETRIC_PRESENTATION_REPRESENTATION('',(#86516),#420);
#67560=STYLED_ITEM ( 'NONE', ( #39661 ), #20554 ) ;
#67736=CARTESIAN_POINT ( 'NONE',  ( 0.000000000000000000, 22.97884757028485225, -55.94820918777160301 ) ) ;
#67755=( NAMED_UNIT ( * ) PLANE_ANGLE_UNIT ( ) SI_UNIT ( $, .RADIAN. ) );
#68292=CARTESIAN_POINT ( 'NONE',  ( 2.892604062750769184E-15, 60.76237703744687479, -11.80995232570204045 ) ) ;
#68620=EDGE_CURVE ( 'NONE', #23946, #74912, #64915, .T. ) ;
#68679=CARTESIAN_POINT ( 'NONE',  ( -23.61990465140407380, 60.76237703744687479, 11.80995232570203690 ) ) ;
#68837=CARTESIAN_POINT ( 'NONE',  ( 55.68167212273443312, 51.11204936430952017, 27.84083606136722722 ) ) ;
#68842=( LENGTH_UNIT ( ) NAMED_UNIT ( * ) SI_UNIT ( .MILLI., .METRE. ) );
#69013=EDGE_CURVE ( 'NONE', #62090, #21078, #106664, .T. ) ;
#69116=ORIENTED_EDGE ( 'NONE', *, *, #77026, .T. ) ;
#69209=CARTESIAN_POINT ( 'NONE',  ( -0.000000000000000000, 60.76237703744687479, -11.80995232570204045 ) ) ;
#69365=CARTESIAN_POINT ( 'NONE',  ( 113.4944653854903862, 14.17434517210798006, -56.74723269274517179 ) ) ;
#69413=FILL_AREA_STYLE ('',( #4673 ) ) ;
#69444=( LENGTH_UNIT ( ) NAMED_UNIT ( * ) SI_UNIT ( .MILLI., .METRE. ) );
#69532=DIRECTION ( 'NONE',  ( 0.000000000000000000, 0.000000000000000000, 1.000000000000000000 ) ) ;
#69677=COLOUR_RGB ( '', 0.72549020, 0.75294118, 0.79215686) ;
#69886=CARTESIAN_POINT ( 'NONE',  ( 2.291854088684162271E-15, 61.34242035161803841, -9.357204421225127078 ) ) ;
#70015=MECHANICAL_DESIGN_GEOMETRIC_PRESENTATION_REPRESENTATION('',(#1058),#4573);
#70121=CARTESIAN_POINT ( 'NONE',  ( -3.409519076813957649E-15, 51.11204936430951307, 27.84083606136722366 ) ) ;
#70422=CARTESIAN_POINT ( 'NONE',  ( -7.499174415388573091E-15, 1.499999999999992450, 61.23540616453487218 ) ) ;
#70427=CARTESIAN_POINT ( 'NONE',  ( 47.33333333333330728, 59.99999999999999289, 23.66666666666666785 ) ) ;
#70469=PRESENTATION_STYLE_ASSIGNMENT (( #86144 ) ) ;
#70572=VERTEX_POINT ( 'NONE', #29692 ) ;
#70784=CARTESIAN_POINT ( 'NONE',  ( -55.68167212273443312, 51.11204936430952017, 27.84083606136721656 ) ) ;
#70831=VERTEX_POINT ( 'NONE', #81243 ) ;
#70906=( LENGTH_UNIT ( ) NAMED_UNIT ( * ) SI_UNIT ( .MILLI., .METRE. ) );
#71007=COLOUR_RGB ( '', 0.09019608, 0.27058824, 0.51372549) ;
#71512=STYLED_ITEM ( 'NONE', ( #102789 ), #22353 ) ;
#71658=AXIS2_PLACEMENT_3D ( 'NONE', #42132, #8704, #75017 ) ;
#72109=DIRECTION ( 'NONE',  ( 0.000000000000000000, 0.000000000000000000, 1.000000000000000000 ) ) ;
#72140=EDGE_CURVE ( 'NONE', #74912, #63111, #79182, .T. ) ;
#72183=PRESENTATION_STYLE_ASSIGNMENT (( #55446 ) ) ;
#72199=CIRCLE ( 'NONE', #30884, 6.999999999999992895 ) ;
#72551=STYLED_ITEM ( 'NONE', ( #105537 ), #19597 ) ;
#72753=CARTESIAN_POINT ( 'NONE',  ( -0.000000000000000000, 7.666536031838887766, -59.53359981990485750 ) ) ;
#72969=( NAMED_UNIT ( * ) SI_UNIT ( $, .STERADIAN. ) SOLID_ANGLE_UNIT ( ) );
#73280=CARTESIAN_POINT ( 'NONE',  ( -7.499174415388573091E-15, 1.499999999999992450, 61.23540616453487218 ) ) ;
#73498=ORIENTED_EDGE ( 'NONE', *, *, #81848, .T. ) ;
#73760=ADVANCED_FACE ( 'NONE', ( #32810, #23657 ), #6365, .T. ) ;
#73824=CARTESIAN_POINT ( 'NONE',  ( -88.26372640434641426, 34.25047185182970111, 44.13186320217319292 ) ) ;
#74402=EDGE_CURVE ( 'NONE', #23078, #45089, #7830, .T. ) ;
#74410=DIRECTION ( 'NONE',  ( 0.000000000000000000, 0.000000000000000000, -1.000000000000000000 ) ) ;
#74429=( BOUNDED_SURFACE ( )  B_SPLINE_SURFACE ( 3, 3, ( 
 ( #25197, #100112, #18157, #26278 ),
 ( #92022, #43484, #24660, #57513 ),
 ( #83930, #16540, #66151, #69886 ),
 ( #21363, #4090, #86626, #68292 ),
 ( #86092, #29466, #28944, #11627 ),
 ( #53693, #52619, #87142, #77445 ),
 ( #20860, #12689, #95232, #85547 ),
 ( #37018, #61818, #62337, #4624 ),
 ( #3014, #68837, #93635, #19786 ),
 ( #101186, #37554, #102244, #35966 ),
 ( #2473, #45094, #3559, #60747 ),
 ( #54203, #45621, #61269, #78493 ),
 ( #19264, #44013, #76902, #85003 ),
 ( #13219, #36497, #76360, #94712 ),
 ( #101715, #35420, #69365, #27347 ),
 ( #77973, #103319, #60225, #12163 ),
 ( #93093, #52093, #11087, #27882 ),
 ( #70422, #44557, #28396, #94159 ) ),
 .UNSPECIFIED., .F., .F., .T. ) 
 B_SPLINE_SURFACE_WITH_KNOTS ( ( 4, 2, 2, 2, 2, 2, 2, 2, 4 ),
 ( 4, 4 ),
 ( 0.000000000000000000, 0.06249999999999997224, 0.1249999999999999445, 0.2500000000000000000, 0.3750000000000000555, 0.5000000000000000000, 0.7500000000000000000, 0.8750000000000000000, 1.000000000000000000 ),
 ( 0.000000000000000000, 1.000000000000000000 ),
 .UNSPECIFIED. ) 
 GEOMETRIC_REPRESENTATION_ITEM ( )  RATIONAL_B_SPLINE_SURFACE ( (
 ( 1.000000000000000000, 0.3333333333333334259, 0.3333333333333334259, 1.000000000000000000),
 ( 1.000000000000000000, 0.3333333333333334259, 0.3333333333333334259, 1.000000000000000000),
 ( 1.000000000000000000, 0.3333333333333334259, 0.3333333333333334259, 1.000000000000000000),
 ( 1.000000000000000000, 0.3333333333333334259, 0.3333333333333334259, 1.000000000000000000),
 ( 1.000000000000000000, 0.3333333333333334259, 0.3333333333333334259, 1.000000000000000000),
 ( 1.000000000000000000, 0.3333333333333334259, 0.3333333333333334259, 1.000000000000000000),
 ( 1.000000000000000000, 0.3333333333333334259, 0.3333333333333334259, 1.000000000000000000),
 ( 1.000000000000000000, 0.3333333333333334259, 0.3333333333333334259, 1.000000000000000000),
 ( 1.000000000000000000, 0.3333333333333334259, 0.3333333333333334259, 1.000000000000000000),
 ( 1.000000000000000000, 0.3333333333333334259, 0.3333333333333334259, 1.000000000000000000),
 ( 1.000000000000000000, 0.3333333333333334259, 0.3333333333333334259, 1.000000000000000000),
 ( 1.000000000000000000, 0.3333333333333334259, 0.3333333333333334259, 1.000000000000000000),
 ( 1.000000000000000000, 0.3333333333333334259, 0.3333333333333334259, 1.000000000000000000),
 ( 1.000000000000000000, 0.3333333333333334259, 0.3333333333333334259, 1.000000000000000000),
 ( 1.000000000000000000, 0.3333333333333334259, 0.3333333333333334259, 1.000000000000000000),
 ( 1.000000000000000000, 0.3333333333333334259, 0.3333333333333334259, 1.000000000000000000),
 ( 1.000000000000000000, 0.3333333333333334259, 0.3333333333333334259, 1.000000000000000000),
 ( 1.000000000000000000, 0.3333333333333334259, 0.3333333333333334259, 1.000000000000000000) ) ) 
 REPRESENTATION_ITEM ( '' )  SURFACE ( )  );
#74801=DIRECTION ( 'NONE',  ( 0.000000000000000000, 1.000000000000000000, 0.000000000000000000 ) ) ;
#74912=VERTEX_POINT ( 'NONE', #20927 ) ;
#74992=( GEOMETRIC_REPRESENTATION_CONTEXT ( 3 ) GLOBAL_UNCERTAINTY_ASSIGNED_CONTEXT ( ( #27616 ) ) GLOBAL_UNIT_ASSIGNED_CONTEXT ( ( #65958, #7706, #72969 ) ) REPRESENTATION_CONTEXT ( 'NONE', 'WORKASPACE' ) );
#75017=DIRECTION ( 'NONE',  ( 0.000000000000000000, 0.000000000000000000, 1.000000000000000000 ) ) ;
#75134=CARTESIAN_POINT ( 'NONE',  ( -1.145927044342081135E-15, 61.34242035161803841, 9.357204421225127078 ) ) ;
#75162=LINE ( 'NONE', #9357, #92629 ) ;
#75769=CARTESIAN_POINT ( 'NONE',  ( -2.898330757982067934E-15, 60.00000000000000000, 23.66666666666665719 ) ) ;
#76206=FILL_AREA_STYLE ('',( #43847 ) ) ;
#76287=ORIENTED_EDGE ( 'NONE', *, *, #69013, .T. ) ;
#76360=CARTESIAN_POINT ( 'NONE',  ( 110.0428892116505040, 17.51648154115788358, -55.02144460582523777 ) ) ;
#76737=CARTESIAN_POINT ( 'NONE',  ( -18.71440884245025060, 61.34242035161803841, 9.357204421225125301 ) ) ;
#76902=CARTESIAN_POINT ( 'NONE',  ( 98.18081844100635180, 27.55047179872464724, -49.09040922050316880 ) ) ;
#77026=EDGE_CURVE ( 'NONE', #45089, #70572, #24012, .T. ) ;
#77445=CARTESIAN_POINT ( 'NONE',  ( 4.143270396293103855E-15, 58.72416816948006613, -16.91618513671782509 ) ) ;
#77447=UNCERTAINTY_MEASURE_WITH_UNIT (LENGTH_MEASURE( 1.000000000000000082E-05 ), #69444, 'distance_accuracy_value', 'NONE');
#77819=CARTESIAN_POINT ( 'NONE',  ( -9.993576133260314080E-16, 61.49999999999999289, 8.160374191332742555 ) ) ;
#77973=CARTESIAN_POINT ( 'NONE',  ( -7.290763246116595115E-15, 7.666536031838887766, 59.53359981990485750 ) ) ;
#78048=CARTESIAN_POINT ( 'NONE',  ( 0.000000000000000000, 0.000000000000000000, 62.00000000000000000 ) ) ;
#78183=AXIS2_PLACEMENT_3D ( 'NONE', #33456, #40462, #74410 ) ;
#78209=CARTESIAN_POINT ( 'NONE',  ( -1.600194386257963230E-15, 60.33964880548970200, 13.06657876680918662 ) ) ;
#78285=CARTESIAN_POINT ( 'NONE',  ( 0.000000000000000000, 60.00000000000000000, 0.000000000000000000 ) ) ;
#78334=CARTESIAN_POINT ( 'NONE',  ( -33.83237027343564307, 58.72416816948007323, -16.91618513671782509 ) ) ;
#78493=CARTESIAN_POINT ( 'NONE',  ( 1.080918900219005715E-14, 34.25047185182970111, -44.13186320217320713 ) ) ;
#78499=CARTESIAN_POINT ( 'NONE',  ( -7.347880794884118356E-15, 0.000000000000000000, 60.00000000000000000 ) ) ;
#78566=DIRECTION ( 'NONE',  ( 0.000000000000000000, 1.000000000000000000, 0.000000000000000000 ) ) ;
#78664=ORIENTED_EDGE ( 'NONE', *, *, #91818, .F. ) ;
#78864=CARTESIAN_POINT ( 'NONE',  ( 0.000000000000000000, 51.11204936430951307, -27.84083606136722366 ) ) ;
#79038=CARTESIAN_POINT ( 'NONE',  ( 13.99999999999998046, 59.99999999999999289, 6.999999999999994671 ) ) ;
#79182=CIRCLE ( 'NONE', #5124, 62.00000000000000000 ) ;
#79358=DIRECTION ( 'NONE',  ( 0.000000000000000000, 1.000000000000000000, 0.000000000000000000 ) ) ;
#79568=SURFACE_STYLE_USAGE ( .BOTH. , #64465 ) ;
#79633=FACE_BOUND ( 'NONE', #18191, .T. ) ;
#79645=( GEOMETRIC_REPRESENTATION_CONTEXT ( 3 ) GLOBAL_UNCERTAINTY_ASSIGNED_CONTEXT ( ( #80140 ) ) GLOBAL_UNIT_ASSIGNED_CONTEXT ( ( #103368, #12212, #13800 ) ) REPRESENTATION_CONTEXT ( 'NONE', 'WORKASPACE' ) );
#79734=UNCERTAINTY_MEASURE_WITH_UNIT (LENGTH_MEASURE( 1.000000000000000082E-05 ), #92927, 'distance_accuracy_value', 'NONE');
#79771=STYLED_ITEM ( 'NONE', ( #48924 ), #21598 ) ;
#80040=CARTESIAN_POINT ( 'NONE',  ( -1.714505518806292863E-15, 60.00000000000000000, 6.999999999999992895 ) ) ;
#80058=COLOUR_RGB ( '', 0.40784314, 0.44705882, 0.49803922) ;
#80140=UNCERTAINTY_MEASURE_WITH_UNIT (LENGTH_MEASURE( 1.000000000000000082E-05 ), #103368, 'distance_accuracy_value', 'NONE');
#80190=FILL_AREA_STYLE_COLOUR ( '', #22696 ) ;
#80850=CARTESIAN_POINT ( 'NONE',  ( -50.10796912846466000, 53.37899725327127953, 25.05398456423233000 ) ) ;
#81103=CARTESIAN_POINT ( 'NONE',  ( -111.8964183755431918, 22.97884757028484870, -55.94820918777161722 ) ) ;
#81243=CARTESIAN_POINT ( 'NONE',  ( -7.499174415388573091E-15, 1.500000000000000444, 61.23540616453487218 ) ) ;
#81245=SURFACE_SIDE_STYLE ('',( #23590 ) ) ;
#81371=CARTESIAN_POINT ( 'NONE',  ( -88.26372640434641426, 34.25047185182970111, -44.13186320217320713 ) ) ;
#81821=FACE_OUTER_BOUND ( 'NONE', #57016, .T. ) ;
#81848=EDGE_CURVE ( 'NONE', #63111, #74912, #7162, .T. ) ;
#81905=CARTESIAN_POINT ( 'NONE',  ( -0.000000000000000000, 17.51648154115788714, -55.02144460582525909 ) ) ;
#82004=ORIENTED_EDGE ( 'NONE', *, *, #10670, .F. ) ;
#82335=SURFACE_STYLE_USAGE ( .BOTH. , #49429 ) ;
#82375=DIRECTION ( 'NONE',  ( 0.000000000000000000, 0.000000000000000000, 1.000000000000000000 ) ) ;
#82454=CARTESIAN_POINT ( 'NONE',  ( -66.76860190796567451, 46.03420836107012093, 33.38430095398283726 ) ) ;
#82715=CARTESIAN_POINT ( 'NONE',  ( -5.404594501095027787E-15, 34.25047185182970111, 44.13186320217320713 ) ) ;
#83396=( NAMED_UNIT ( * ) SI_UNIT ( $, .STERADIAN. ) SOLID_ANGLE_UNIT ( ) );
#83926=EDGE_LOOP ( 'NONE', ( #96522, #95145, #2711, #56891 ) ) ;
#83930=CARTESIAN_POINT ( 'NONE',  ( -1.145927044342081135E-15, 61.34242035161803841, 9.357204421225127078 ) ) ;
#84843=PRESENTATION_STYLE_ASSIGNMENT (( #44935 ) ) ;
#84897=MECHANICAL_DESIGN_GEOMETRIC_PRESENTATION_REPRESENTATION('',(#90042),#79645);
#84947=AXIS2_PLACEMENT_3D ( 'NONE', #89422, #105585, #57549 ) ;
#85003=CARTESIAN_POINT ( 'NONE',  ( 1.202368250414458695E-14, 27.55047179872464724, -49.09040922050319011 ) ) ;
#85224=( GEOMETRIC_REPRESENTATION_CONTEXT ( 3 ) GLOBAL_UNCERTAINTY_ASSIGNED_CONTEXT ( ( #97862 ) ) GLOBAL_UNIT_ASSIGNED_CONTEXT ( ( #68842, #28950, #12695 ) ) REPRESENTATION_CONTEXT ( 'NONE', 'WORKASPACE' ) );
#85290=CARTESIAN_POINT ( 'NONE',  ( 8.572527594031464315E-16, 61.50000000000000000, -6.999999999999992895 ) ) ;
#85547=CARTESIAN_POINT ( 'NONE',  ( 4.798419095149803646E-15, 57.18445727710329862, -19.59103268995865221 ) ) ;
#85932=CARTESIAN_POINT ( 'NONE',  ( -0.000000000000000000, 61.49999999999999289, -8.160374191332742555 ) ) ;
#86092=CARTESIAN_POINT ( 'NONE',  ( -1.600194386257963230E-15, 60.33964880548970200, 13.06657876680918662 ) ) ;
#86144=SURFACE_STYLE_USAGE ( .BOTH. , #30026 ) ;
#86297=PRODUCT_DEFINITION_SHAPE ( 'NONE', 'NONE',  #27211 ) ;
#86369=AXIS2_PLACEMENT_3D ( 'NONE', #22537, #39235, #72109 ) ;
#86468=CARTESIAN_POINT ( 'NONE',  ( -1.145927044342081333E-15, 61.34242035161803841, 9.357204421225127078 ) ) ;
#86516=STYLED_ITEM ( 'NONE', ( #97012 ), #51736 ) ;
#86626=CARTESIAN_POINT ( 'NONE',  ( 23.61990465140407736, 60.76237703744687479, -11.80995232570203690 ) ) ;
#86631=CARTESIAN_POINT ( 'NONE',  ( 1.370335905996620722E-14, 22.97884757028485225, -55.94820918777160301 ) ) ;
#86796=AXIS2_PLACEMENT_3D ( 'NONE', #88666, #5099, #4034 ) ;
#86984=CARTESIAN_POINT ( 'NONE',  ( -119.0671996398097008, 7.666536031838888654, -59.53359981990485750 ) ) ;
#87106=PRESENTATION_STYLE_ASSIGNMENT (( #45583 ) ) ;
#87142=CARTESIAN_POINT ( 'NONE',  ( 33.83237027343565018, 58.72416816948007323, -16.91618513671781798 ) ) ;
#87156=CARTESIAN_POINT ( 'NONE',  ( 0.000000000000000000, 14.17434517210798184, -56.74723269274520021 ) ) ;
#87216=PLANE ( 'NONE',  #63084 ) ;
#87597=VECTOR ( 'NONE', #50305, 1000.000000000000000 ) ;
#87676=CARTESIAN_POINT ( 'NONE',  ( 119.9999999999999432, 0.000000000000000000, 60.00000000000001421 ) ) ;
#87873=( LENGTH_UNIT ( ) NAMED_UNIT ( * ) SI_UNIT ( .MILLI., .METRE. ) );
#88157=CARTESIAN_POINT ( 'NONE',  ( 8.572527594031464315E-16, 60.00000000000000000, -6.999999999999992895 ) ) ;
#88666=CARTESIAN_POINT ( 'NONE',  ( 0.000000000000000000, 0.000000000000000000, 0.000000000000000000 ) ) ;
#88731=FACE_OUTER_BOUND ( 'NONE', #64045, .T. ) ;
#88740=PRODUCT_DEFINITION_FORMATION_WITH_SPECIFIED_SOURCE ( 'ANY', '', #12205, .NOT_KNOWN. ) ;
#88942=CARTESIAN_POINT ( 'NONE',  ( -7.347880794884119933E-15, 0.000000000000000000, 60.00000000000000000 ) ) ;
#88959=CARTESIAN_POINT ( 'NONE',  ( 0.000000000000000000, 1.499999999999992450, -61.23540616453487218 ) ) ;
#89263=( LENGTH_UNIT ( ) NAMED_UNIT ( * ) SI_UNIT ( .MILLI., .METRE. ) );
#89333=APPLICATION_CONTEXT ( 'automotive_design' ) ;
#89422=CARTESIAN_POINT ( 'NONE',  ( 0.000000000000000000, 0.000000000000000000, 0.000000000000000000 ) ) ;
#89491=ORIENTED_EDGE ( 'NONE', *, *, #77026, .F. ) ;
#89493=CARTESIAN_POINT ( 'NONE',  ( -66.76860190796567451, 46.03420836107012093, -33.38430095398284436 ) ) ;
#90042=STYLED_ITEM ( 'NONE', ( #70469 ), #19059 ) ;
#90063=AXIS2_PLACEMENT_3D ( 'NONE', #7147, #89, #33058 ) ;
#90270=CARTESIAN_POINT ( 'NONE',  ( 6.851679529983103610E-15, 22.97884757028485225, -55.94820918777160301 ) ) ;
#90337=EDGE_CURVE ( 'NONE', #23078, #6036, #72199, .T. ) ;
#90774=FACE_OUTER_BOUND ( 'NONE', #54008, .T. ) ;
#90809=CARTESIAN_POINT ( 'NONE',  ( -111.8964183755431918, 22.97884757028484870, 55.94820918777157459 ) ) ;
#90950=DIRECTION ( 'NONE',  ( 0.000000000000000000, 1.000000000000000000, 0.000000000000000000 ) ) ;
#91391=APPLICATION_CONTEXT ( 'automotive_design' ) ;
#91508=FILL_AREA_STYLE_COLOUR ( '', #69677 ) ;
#91579=MECHANICAL_DESIGN_GEOMETRIC_PRESENTATION_REPRESENTATION('',(#72551),#45091);
#91818=EDGE_CURVE ( 'NONE', #6036, #21078, #31378, .T. ) ;
#91867=AXIS2_PLACEMENT_3D ( 'NONE', #35324, #74801, #82375 ) ;
#92021=PRODUCT_DEFINITION_CONTEXT ( 'detailed design', #91391, 'design' ) ;
#92022=CARTESIAN_POINT ( 'NONE',  ( -9.993576133260312108E-16, 61.49999999999999289, 8.160374191332742555 ) ) ;
#92169=EDGE_LOOP ( 'NONE', ( #9944, #57989, #16810, #9132 ) ) ;
#92523=DIRECTION ( 'NONE',  ( 0.000000000000000000, 0.000000000000000000, 1.000000000000000000 ) ) ;
#92629=VECTOR ( 'NONE', #50354, 1000.000000000000000 ) ;
#92927=( LENGTH_UNIT ( ) NAMED_UNIT ( * ) SI_UNIT ( .MILLI., .METRE. ) );
#92959=ORIENTED_EDGE ( 'NONE', *, *, #68620, .T. ) ;
#93093=CARTESIAN_POINT ( 'NONE',  ( -7.420756919583588009E-15, 4.501353321498349658, 60.59507871780017751 ) ) ;
#93479=CARTESIAN_POINT ( 'NONE',  ( -26.13315753361836613, 60.33964880548970910, 13.06657876680918307 ) ) ;
#93578=( GEOMETRIC_REPRESENTATION_CONTEXT ( 3 ) GLOBAL_UNCERTAINTY_ASSIGNED_CONTEXT ( ( #55786 ) ) GLOBAL_UNIT_ASSIGNED_CONTEXT ( ( #40850, #99074, #50007 ) ) REPRESENTATION_CONTEXT ( 'NONE', 'WORKASPACE' ) );
#93635=CARTESIAN_POINT ( 'NONE',  ( 55.68167212273443312, 51.11204936430952017, -27.84083606136720945 ) ) ;
#94159=CARTESIAN_POINT ( 'NONE',  ( 1.499834883077714618E-14, 1.499999999999992450, -61.23540616453487218 ) ) ;
#94712=CARTESIAN_POINT ( 'NONE',  ( 1.347636720419746323E-14, 17.51648154115788714, -55.02144460582525909 ) ) ;
#94949=CARTESIAN_POINT ( 'NONE',  ( -4.425930005958662145E-15, 43.22324503868515677, 36.14046114390016839 ) ) ;
#95027=DIRECTION ( 'NONE',  ( 0.000000000000000000, 0.000000000000000000, 1.000000000000000000 ) ) ;
#95076=CARTESIAN_POINT ( 'NONE',  ( 0.000000000000000000, 27.55047179872464724, -49.09040922050319011 ) ) ;
#95145=ORIENTED_EDGE ( 'NONE', *, *, #74402, .T. ) ;
#95232=CARTESIAN_POINT ( 'NONE',  ( 39.18206537991730443, 57.18445727710330573, -19.59103268995864155 ) ) ;
#95453=( GEOMETRIC_REPRESENTATION_CONTEXT ( 3 ) GLOBAL_UNCERTAINTY_ASSIGNED_CONTEXT ( ( #22237 ) ) GLOBAL_UNIT_ASSIGNED_CONTEXT ( ( #98513, #67755, #83396 ) ) REPRESENTATION_CONTEXT ( 'NONE', 'WORKASPACE' ) );
#95759=CARTESIAN_POINT ( 'NONE',  ( 1.714505518806292863E-15, 60.00000000000000000, -6.999999999999992895 ) ) ;
#95871=FACE_OUTER_BOUND ( 'NONE', #44813, .T. ) ;
#96262=SURFACE_SIDE_STYLE ('',( #5633 ) ) ;
#96308=DIRECTION ( 'NONE',  ( 0.000000000000000000, 1.000000000000000000, 0.000000000000000000 ) ) ;
#96471=FILL_AREA_STYLE_COLOUR ( '', #36423 ) ;
#96522=ORIENTED_EDGE ( 'NONE', *, *, #14632, .T. ) ;
#96832=CARTESIAN_POINT ( 'NONE',  ( -0.000000000000000000, 7.666536031838887766, -59.53359981990485750 ) ) ;
#96990=( NAMED_UNIT ( * ) SI_UNIT ( $, .STERADIAN. ) SOLID_ANGLE_UNIT ( ) );
#97012=PRESENTATION_STYLE_ASSIGNMENT (( #37761 ) ) ;
#97039=CARTESIAN_POINT ( 'NONE',  ( -121.1901574356003550, 4.501353321498349658, 60.59507871780017041 ) ) ;
#97340=STYLED_ITEM ( 'NONE', ( #24994 ), #99188 ) ;
#97556=CARTESIAN_POINT ( 'NONE',  ( -98.18081844100633759, 27.55047179872464724, -49.09040922050319011 ) ) ;
#97806=SURFACE_STYLE_FILL_AREA ( #29541 ) ;
#97821=CARTESIAN_POINT ( 'NONE',  ( -119.9999999999999858, 0.000000000000000000, 59.99999999999997158 ) ) ;
#97862=UNCERTAINTY_MEASURE_WITH_UNIT (LENGTH_MEASURE( 1.000000000000000082E-05 ), #68842, 'distance_accuracy_value', 'NONE');
#97909=STYLED_ITEM ( 'NONE', ( #84843 ), #41411 ) ;
#98102=CARTESIAN_POINT ( 'NONE',  ( -113.4944653854903862, 14.17434517210798006, 56.74723269274519311 ) ) ;
#98513=( LENGTH_UNIT ( ) NAMED_UNIT ( * ) SI_UNIT ( .MILLI., .METRE. ) );
#98517=ORIENTED_EDGE ( 'NONE', *, *, #2691, .T. ) ;
#98993=( BOUNDED_SURFACE ( )  B_SPLINE_SURFACE ( 3, 3, ( 
 ( #45625, #79038, #37561, #95759 ),
 ( #21898, #70427, #13756, #54743 ),
 ( #103323, #38089, #103839, #86631 ),
 ( #78499, #87676, #60753, #29471 ) ),
 .UNSPECIFIED., .F., .F., .T. ) 
 B_SPLINE_SURFACE_WITH_KNOTS ( ( 4, 4 ),
 ( 4, 4 ),
 ( 0.000000000000000000, 1.000000000000000000 ),
 ( 0.000000000000000000, 1.000000000000000000 ),
 .UNSPECIFIED. ) 
 GEOMETRIC_REPRESENTATION_ITEM ( )  RATIONAL_B_SPLINE_SURFACE ( (
 ( 1.000000000000000000, 0.3333333333333334259, 0.3333333333333334259, 1.000000000000000000),
 ( 1.000000000000000000, 0.3333333333333334259, 0.3333333333333334259, 1.000000000000000000),
 ( 1.000000000000000000, 0.3333333333333334259, 0.3333333333333334259, 1.000000000000000000),
 ( 1.000000000000000000, 0.3333333333333334259, 0.3333333333333334259, 1.000000000000000000) ) ) 
 REPRESENTATION_ITEM ( '' )  SURFACE ( )  );
#99049=UNCERTAINTY_MEASURE_WITH_UNIT (LENGTH_MEASURE( 1.000000000000000082E-05 ), #6295, 'distance_accuracy_value', 'NONE');
#99074=( NAMED_UNIT ( * ) PLANE_ANGLE_UNIT ( ) SI_UNIT ( $, .RADIAN. ) );
#99188=ADVANCED_FACE ( 'NONE', ( #90774 ), #64382, .T. ) ;
#99405=CARTESIAN_POINT ( 'NONE',  ( -7.420756919583588009E-15, 4.501353321498349658, 60.59507871780017751 ) ) ;
#100112=CARTESIAN_POINT ( 'NONE',  ( 13.99999999999998046, 61.49999999999999289, 6.999999999999994671 ) ) ;
#100320=UNCERTAINTY_MEASURE_WITH_UNIT (LENGTH_MEASURE( 1.000000000000000082E-05 ), #34411, 'distance_accuracy_value', 'NONE');
#100369=CIRCLE ( 'NONE', #90063, 61.23540616453487218 ) ;
#100615=CARTESIAN_POINT ( 'NONE',  ( 0.000000000000000000, 0.000000000000000000, 0.000000000000000000 ) ) ;
#100630=ORIENTED_EDGE ( 'NONE', *, *, #52910, .T. ) ;
#101020=CARTESIAN_POINT ( 'NONE',  ( -13.99999999999998046, 61.49999999999999289, 6.999999999999990230 ) ) ;
#101186=CARTESIAN_POINT ( 'NONE',  ( -4.088397730506703845E-15, 46.03420836107012093, 33.38430095398285147 ) ) ;
#101384=( GEOMETRIC_REPRESENTATION_CONTEXT ( 3 ) GLOBAL_UNCERTAINTY_ASSIGNED_CONTEXT ( ( #79734 ) ) GLOBAL_UNIT_ASSIGNED_CONTEXT ( ( #92927, #28239, #10410 ) ) REPRESENTATION_CONTEXT ( 'NONE', 'WORKASPACE' ) );
#101393=VECTOR ( 'NONE', #78566, 1000.000000000000000 ) ;
#101560=CARTESIAN_POINT ( 'NONE',  ( -1.446302031375384395E-15, 60.76237703744687479, 11.80995232570204045 ) ) ;
#101563=ORIENTED_EDGE ( 'NONE', *, *, #74402, .F. ) ;
#101715=CARTESIAN_POINT ( 'NONE',  ( -6.949531687764044400E-15, 14.17434517210798184, 56.74723269274520021 ) ) ;
#101806=AXIS2_PLACEMENT_3D ( 'NONE', #16062, #106660, #56509 ) ;
#102077=CARTESIAN_POINT ( 'NONE',  ( -23.61990465140407380, 60.76237703744687479, -11.80995232570204223 ) ) ;
#102124=ORIENTED_EDGE ( 'NONE', *, *, #57377, .F. ) ;
#102244=CARTESIAN_POINT ( 'NONE',  ( 66.76860190796568872, 46.03420836107012093, -33.38430095398283726 ) ) ;
#102250=FILL_AREA_STYLE ('',( #5159 ) ) ;
#102591=DIRECTION ( 'NONE',  ( 0.000000000000000000, 0.000000000000000000, -1.000000000000000000 ) ) ;
#102789=PRESENTATION_STYLE_ASSIGNMENT (( #28401 ) ) ;
#103319=CARTESIAN_POINT ( 'NONE',  ( 119.0671996398096724, 7.666536031838888654, 59.53359981990487171 ) ) ;
#103323=CARTESIAN_POINT ( 'NONE',  ( -6.851679529983103610E-15, 22.97884757028485225, 55.94820918777160301 ) ) ;
#103324=CARTESIAN_POINT ( 'NONE',  ( 0.000000000000000000, 1.500000000000000000, 0.000000000000000000 ) ) ;
#103368=( LENGTH_UNIT ( ) NAMED_UNIT ( * ) SI_UNIT ( .MILLI., .METRE. ) );
#103391=DIRECTION ( 'NONE',  ( 0.000000000000000000, -0.000000000000000000, 1.000000000000000000 ) ) ;
#103585=STYLED_ITEM ( 'NONE', ( #72183 ), #73760 ) ;
#103679=CARTESIAN_POINT ( 'NONE',  ( -6.738183602098730825E-15, 17.51648154115788714, 55.02144460582525909 ) ) ;
#103839=CARTESIAN_POINT ( 'NONE',  ( 111.8964183755431918, 22.97884757028484870, -55.94820918777157459 ) ) ;
#103842=CYLINDRICAL_SURFACE ( 'NONE', #60716, 6.999999999999992895 ) ;
#103909=PRESENTATION_STYLE_ASSIGNMENT (( #32041 ) ) ;
#104321=( NAMED_UNIT ( * ) SI_UNIT ( $, .STERADIAN. ) SOLID_ANGLE_UNIT ( ) );
#104373=CARTESIAN_POINT ( 'NONE',  ( 0.000000000000000000, 57.18445727710329862, -19.59103268995865221 ) ) ;
#104437=( NAMED_UNIT ( * ) SI_UNIT ( $, .STERADIAN. ) SOLID_ANGLE_UNIT ( ) );
#104474=CYLINDRICAL_SURFACE ( 'NONE', #86369, 6.999999999999992895 ) ;
#104868=CARTESIAN_POINT ( 'NONE',  ( -13.99999999999998401, 59.99999999999999289, 6.999999999999989342 ) ) ;
#104893=ORIENTED_EDGE ( 'NONE', *, *, #54811, .T. ) ;
#104928=CARTESIAN_POINT ( 'NONE',  ( 0.000000000000000000, 61.34242035161803841, -9.357204421225127078 ) ) ;
#105125=CARTESIAN_POINT ( 'NONE',  ( 0.000000000000000000, 0.000000000000000000, 62.00000000000000000 ) ) ;
#105305=ORIENTED_EDGE ( 'NONE', *, *, #81848, .F. ) ;
#105496=( GEOMETRIC_REPRESENTATION_CONTEXT ( 3 ) GLOBAL_UNCERTAINTY_ASSIGNED_CONTEXT ( ( #59015 ) ) GLOBAL_UNIT_ASSIGNED_CONTEXT ( ( #89263, #38604, #15361 ) ) REPRESENTATION_CONTEXT ( 'NONE', 'WORKASPACE' ) );
#105537=PRESENTATION_STYLE_ASSIGNMENT (( #56437 ) ) ;
#105585=DIRECTION ( 'NONE',  ( 0.000000000000000000, 1.000000000000000000, 0.000000000000000000 ) ) ;
#105602=SURFACE_STYLE_FILL_AREA ( #40875 ) ;
#105659=CARTESIAN_POINT ( 'NONE',  ( -2.399209547574902217E-15, 57.18445727710329862, 19.59103268995865221 ) ) ;
#105958=CARTESIAN_POINT ( 'NONE',  ( 0.000000000000000000, 60.33964880548970200, -13.06657876680918662 ) ) ;
#106660=DIRECTION ( 'NONE',  ( 0.000000000000000000, 1.000000000000000000, 0.000000000000000000 ) ) ;
#106664=CIRCLE ( 'NONE', #65328, 6.999999999999992895 ) ;
#106719=CARTESIAN_POINT ( 'NONE',  ( -6.011841252072293477E-15, 27.55047179872464724, 49.09040922050319011 ) ) ;
ENDSEC;
END-ISO-10303-21;
